ISO-10303-21;
HEADER;
/* Generated by software containing ST-Developer
 * from STEP Tools, Inc. (www.steptools.com) 
 */

FILE_DESCRIPTION(
/* description */ ('Bracket-mounted idler roller'),
/* implementation_level */ '2;1');

FILE_NAME(
/* name */ 'Bearing insert (1).step',
/* time_stamp */ '2026-10-28T03:26:42-07:00',
/* author */ (''),
/* organization */ (''),
/* preprocessor_version */ 'ST-DEVELOPER v20.2',
/* originating_system */ 'Autodesk Translation Framework v15.17.0.0',
/* authorisation */ '');

FILE_SCHEMA (('AUTOMOTIVE_DESIGN { 1 0 10303 214 3 1 1 }'));
ENDSEC;

DATA;
#10=MECHANICAL_DESIGN_GEOMETRIC_PRESENTATION_REPRESENTATION('',(#305),#6241);
#255=SHAPE_REPRESENTATION_RELATIONSHIP('SRR','None',#6361,#276);
#276=ADVANCED_BREP_SHAPE_REPRESENTATION('',(#333),#6237);
#305=STYLED_ITEM('',(#6538),#333);
#333=MANIFOLD_SOLID_BREP('Body1',#3208);
#393=FACE_BOUND('',#922,.T.);
#394=FACE_BOUND('',#926,.T.);
#395=FACE_BOUND('',#927,.T.);
#396=FACE_BOUND('',#928,.T.);
#397=FACE_BOUND('',#929,.T.);
#398=FACE_BOUND('',#930,.T.);
#399=FACE_BOUND('',#932,.T.);
#400=FACE_BOUND('',#933,.T.);
#401=FACE_BOUND('',#934,.T.);
#402=FACE_BOUND('',#935,.T.);
#403=FACE_BOUND('',#936,.T.);
#498=PLANE('',#3782);
#499=PLANE('',#3789);
#500=PLANE('',#3790);
#668=FACE_OUTER_BOUND('',#916,.T.);
#669=FACE_OUTER_BOUND('',#917,.T.);
#670=FACE_OUTER_BOUND('',#918,.T.);
#671=FACE_OUTER_BOUND('',#919,.T.);
#672=FACE_OUTER_BOUND('',#920,.T.);
#673=FACE_OUTER_BOUND('',#921,.T.);
#674=FACE_OUTER_BOUND('',#923,.T.);
#675=FACE_OUTER_BOUND('',#924,.T.);
#676=FACE_OUTER_BOUND('',#925,.T.);
#677=FACE_OUTER_BOUND('',#931,.T.);
#916=EDGE_LOOP('',(#2774,#2775,#2776,#2777));
#917=EDGE_LOOP('',(#2778,#2779,#2780,#2781));
#918=EDGE_LOOP('',(#2782,#2783,#2784,#2785));
#919=EDGE_LOOP('',(#2786,#2787,#2788,#2789));
#920=EDGE_LOOP('',(#2790,#2791,#2792,#2793));
#921=EDGE_LOOP('',(#2794));
#922=EDGE_LOOP('',(#2795));
#923=EDGE_LOOP('',(#2796,#2797,#2798,#2799));
#924=EDGE_LOOP('',(#2800,#2801,#2802,#2803));
#925=EDGE_LOOP('',(#2804));
#926=EDGE_LOOP('',(#2805));
#927=EDGE_LOOP('',(#2806));
#928=EDGE_LOOP('',(#2807));
#929=EDGE_LOOP('',(#2808));
#930=EDGE_LOOP('',(#2809));
#931=EDGE_LOOP('',(#2810));
#932=EDGE_LOOP('',(#2811));
#933=EDGE_LOOP('',(#2812));
#934=EDGE_LOOP('',(#2813));
#935=EDGE_LOOP('',(#2814));
#936=EDGE_LOOP('',(#2815));
#1122=LINE('',#5986,#1304);
#1123=LINE('',#5992,#1305);
#1124=LINE('',#5998,#1306);
#1125=LINE('',#6004,#1307);
#1126=LINE('',#6010,#1308);
#1127=LINE('',#6018,#1309);
#1128=LINE('',#6023,#1310);
#1304=VECTOR('',#4677,0.165);
#1305=VECTOR('',#4684,0.165);
#1306=VECTOR('',#4691,0.165);
#1307=VECTOR('',#4698,0.165);
#1308=VECTOR('',#4705,1.2);
#1309=VECTOR('',#4716,1.5);
#1310=VECTOR('',#4721,2.2);
#1486=CIRCLE('',#3768,0.165);
#1487=CIRCLE('',#3769,0.165);
#1488=CIRCLE('',#3771,0.165);
#1489=CIRCLE('',#3772,0.165);
#1490=CIRCLE('',#3774,0.165);
#1491=CIRCLE('',#3775,0.165);
#1492=CIRCLE('',#3777,0.165);
#1493=CIRCLE('',#3778,0.165);
#1494=CIRCLE('',#3780,1.2);
#1495=CIRCLE('',#3781,1.2);
#1496=CIRCLE('',#3783,1.5);
#1497=CIRCLE('',#3785,1.5);
#1498=CIRCLE('',#3787,2.2);
#1499=CIRCLE('',#3788,2.2);
#1735=VERTEX_POINT('',#5983);
#1736=VERTEX_POINT('',#5985);
#1737=VERTEX_POINT('',#5989);
#1738=VERTEX_POINT('',#5991);
#1739=VERTEX_POINT('',#5995);
#1740=VERTEX_POINT('',#5997);
#1741=VERTEX_POINT('',#6001);
#1742=VERTEX_POINT('',#6003);
#1743=VERTEX_POINT('',#6007);
#1744=VERTEX_POINT('',#6009);
#1745=VERTEX_POINT('',#6013);
#1746=VERTEX_POINT('',#6016);
#1747=VERTEX_POINT('',#6020);
#1748=VERTEX_POINT('',#6022);
#2089=EDGE_CURVE('',#1735,#1735,#1486,.T.);
#2090=EDGE_CURVE('',#1735,#1736,#1122,.T.);
#2091=EDGE_CURVE('',#1736,#1736,#1487,.T.);
#2092=EDGE_CURVE('',#1737,#1737,#1488,.T.);
#2093=EDGE_CURVE('',#1737,#1738,#1123,.T.);
#2094=EDGE_CURVE('',#1738,#1738,#1489,.T.);
#2095=EDGE_CURVE('',#1739,#1739,#1490,.T.);
#2096=EDGE_CURVE('',#1739,#1740,#1124,.T.);
#2097=EDGE_CURVE('',#1740,#1740,#1491,.T.);
#2098=EDGE_CURVE('',#1741,#1741,#1492,.T.);
#2099=EDGE_CURVE('',#1741,#1742,#1125,.T.);
#2100=EDGE_CURVE('',#1742,#1742,#1493,.T.);
#2101=EDGE_CURVE('',#1743,#1743,#1494,.T.);
#2102=EDGE_CURVE('',#1743,#1744,#1126,.T.);
#2103=EDGE_CURVE('',#1744,#1744,#1495,.T.);
#2104=EDGE_CURVE('',#1745,#1745,#1496,.T.);
#2105=EDGE_CURVE('',#1746,#1746,#1497,.T.);
#2106=EDGE_CURVE('',#1746,#1745,#1127,.T.);
#2107=EDGE_CURVE('',#1747,#1747,#1498,.T.);
#2108=EDGE_CURVE('',#1747,#1748,#1128,.T.);
#2109=EDGE_CURVE('',#1748,#1748,#1499,.T.);
#2774=ORIENTED_EDGE('',*,*,#2089,.F.);
#2775=ORIENTED_EDGE('',*,*,#2090,.T.);
#2776=ORIENTED_EDGE('',*,*,#2091,.F.);
#2777=ORIENTED_EDGE('',*,*,#2090,.F.);
#2778=ORIENTED_EDGE('',*,*,#2092,.F.);
#2779=ORIENTED_EDGE('',*,*,#2093,.T.);
#2780=ORIENTED_EDGE('',*,*,#2094,.F.);
#2781=ORIENTED_EDGE('',*,*,#2093,.F.);
#2782=ORIENTED_EDGE('',*,*,#2095,.F.);
#2783=ORIENTED_EDGE('',*,*,#2096,.T.);
#2784=ORIENTED_EDGE('',*,*,#2097,.F.);
#2785=ORIENTED_EDGE('',*,*,#2096,.F.);
#2786=ORIENTED_EDGE('',*,*,#2098,.F.);
#2787=ORIENTED_EDGE('',*,*,#2099,.T.);
#2788=ORIENTED_EDGE('',*,*,#2100,.F.);
#2789=ORIENTED_EDGE('',*,*,#2099,.F.);
#2790=ORIENTED_EDGE('',*,*,#2101,.F.);
#2791=ORIENTED_EDGE('',*,*,#2102,.T.);
#2792=ORIENTED_EDGE('',*,*,#2103,.T.);
#2793=ORIENTED_EDGE('',*,*,#2102,.F.);
#2794=ORIENTED_EDGE('',*,*,#2104,.F.);
#2795=ORIENTED_EDGE('',*,*,#2101,.T.);
#2796=ORIENTED_EDGE('',*,*,#2105,.F.);
#2797=ORIENTED_EDGE('',*,*,#2106,.T.);
#2798=ORIENTED_EDGE('',*,*,#2104,.T.);
#2799=ORIENTED_EDGE('',*,*,#2106,.F.);
#2800=ORIENTED_EDGE('',*,*,#2107,.F.);
#2801=ORIENTED_EDGE('',*,*,#2108,.T.);
#2802=ORIENTED_EDGE('',*,*,#2109,.T.);
#2803=ORIENTED_EDGE('',*,*,#2108,.F.);
#2804=ORIENTED_EDGE('',*,*,#2107,.T.);
#2805=ORIENTED_EDGE('',*,*,#2105,.T.);
#2806=ORIENTED_EDGE('',*,*,#2100,.T.);
#2807=ORIENTED_EDGE('',*,*,#2097,.T.);
#2808=ORIENTED_EDGE('',*,*,#2094,.T.);
#2809=ORIENTED_EDGE('',*,*,#2091,.T.);
#2810=ORIENTED_EDGE('',*,*,#2109,.F.);
#2811=ORIENTED_EDGE('',*,*,#2103,.F.);
#2812=ORIENTED_EDGE('',*,*,#2098,.T.);
#2813=ORIENTED_EDGE('',*,*,#2095,.T.);
#2814=ORIENTED_EDGE('',*,*,#2092,.T.);
#2815=ORIENTED_EDGE('',*,*,#2089,.T.);
#2974=CYLINDRICAL_SURFACE('',#3767,0.165);
#2975=CYLINDRICAL_SURFACE('',#3770,0.165);
#2976=CYLINDRICAL_SURFACE('',#3773,0.165);
#2977=CYLINDRICAL_SURFACE('',#3776,0.165);
#2978=CYLINDRICAL_SURFACE('',#3779,1.2);
#2979=CYLINDRICAL_SURFACE('',#3784,1.5);
#2980=CYLINDRICAL_SURFACE('',#3786,2.2);
#3143=ADVANCED_FACE('',(#668),#2974,.F.);
#3144=ADVANCED_FACE('',(#669),#2975,.F.);
#3145=ADVANCED_FACE('',(#670),#2976,.F.);
#3146=ADVANCED_FACE('',(#671),#2977,.F.);
#3147=ADVANCED_FACE('',(#672),#2978,.F.);
#3148=ADVANCED_FACE('',(#673,#393),#498,.T.);
#3149=ADVANCED_FACE('',(#674),#2979,.F.);
#3150=ADVANCED_FACE('',(#675),#2980,.T.);
#3151=ADVANCED_FACE('',(#676,#394,#395,#396,#397,#398),#499,.T.);
#3152=ADVANCED_FACE('',(#677,#399,#400,#401,#402,#403),#500,.F.);
#3208=CLOSED_SHELL('',(#3143,#3144,#3145,#3146,#3147,#3148,#3149,#3150,
#3151,#3152));
#3766=AXIS2_PLACEMENT_3D('',#5981,#4671,#4672);
#3767=AXIS2_PLACEMENT_3D('',#5982,#4673,#4674);
#3768=AXIS2_PLACEMENT_3D('',#5984,#4675,#4676);
#3769=AXIS2_PLACEMENT_3D('',#5987,#4678,#4679);
#3770=AXIS2_PLACEMENT_3D('',#5988,#4680,#4681);
#3771=AXIS2_PLACEMENT_3D('',#5990,#4682,#4683);
#3772=AXIS2_PLACEMENT_3D('',#5993,#4685,#4686);
#3773=AXIS2_PLACEMENT_3D('',#5994,#4687,#4688);
#3774=AXIS2_PLACEMENT_3D('',#5996,#4689,#4690);
#3775=AXIS2_PLACEMENT_3D('',#5999,#4692,#4693);
#3776=AXIS2_PLACEMENT_3D('',#6000,#4694,#4695);
#3777=AXIS2_PLACEMENT_3D('',#6002,#4696,#4697);
#3778=AXIS2_PLACEMENT_3D('',#6005,#4699,#4700);
#3779=AXIS2_PLACEMENT_3D('',#6006,#4701,#4702);
#3780=AXIS2_PLACEMENT_3D('',#6008,#4703,#4704);
#3781=AXIS2_PLACEMENT_3D('',#6011,#4706,#4707);
#3782=AXIS2_PLACEMENT_3D('',#6012,#4708,#4709);
#3783=AXIS2_PLACEMENT_3D('',#6014,#4710,#4711);
#3784=AXIS2_PLACEMENT_3D('',#6015,#4712,#4713);
#3785=AXIS2_PLACEMENT_3D('',#6017,#4714,#4715);
#3786=AXIS2_PLACEMENT_3D('',#6019,#4717,#4718);
#3787=AXIS2_PLACEMENT_3D('',#6021,#4719,#4720);
#3788=AXIS2_PLACEMENT_3D('',#6024,#4722,#4723);
#3789=AXIS2_PLACEMENT_3D('',#6025,#4724,#4725);
#3790=AXIS2_PLACEMENT_3D('',#6026,#4726,#4727);
#4671=DIRECTION('axis',(0.,0.,1.));
#4672=DIRECTION('refdir',(1.,0.,0.));
#4673=DIRECTION('center_axis',(0.,1.,0.));
#4674=DIRECTION('ref_axis',(1.,0.,0.));
#4675=DIRECTION('center_axis',(0.,1.,0.));
#4676=DIRECTION('ref_axis',(1.,0.,0.));
#4677=DIRECTION('',(0.,1.,0.));
#4678=DIRECTION('center_axis',(0.,-1.,0.));
#4679=DIRECTION('ref_axis',(1.,0.,0.));
#4680=DIRECTION('center_axis',(0.,1.,0.));
#4681=DIRECTION('ref_axis',(1.,0.,0.));
#4682=DIRECTION('center_axis',(0.,1.,0.));
#4683=DIRECTION('ref_axis',(1.,0.,0.));
#4684=DIRECTION('',(0.,1.,0.));
#4685=DIRECTION('center_axis',(0.,-1.,0.));
#4686=DIRECTION('ref_axis',(1.,0.,0.));
#4687=DIRECTION('center_axis',(0.,1.,0.));
#4688=DIRECTION('ref_axis',(1.,0.,0.));
#4689=DIRECTION('center_axis',(0.,1.,0.));
#4690=DIRECTION('ref_axis',(1.,0.,0.));
#4691=DIRECTION('',(0.,1.,0.));
#4692=DIRECTION('center_axis',(0.,-1.,0.));
#4693=DIRECTION('ref_axis',(1.,0.,0.));
#4694=DIRECTION('center_axis',(0.,1.,0.));
#4695=DIRECTION('ref_axis',(1.,0.,0.));
#4696=DIRECTION('center_axis',(0.,1.,0.));
#4697=DIRECTION('ref_axis',(1.,0.,0.));
#4698=DIRECTION('',(0.,1.,0.));
#4699=DIRECTION('center_axis',(0.,-1.,0.));
#4700=DIRECTION('ref_axis',(1.,0.,0.));
#4701=DIRECTION('center_axis',(0.,1.,0.));
#4702=DIRECTION('ref_axis',(1.,0.,0.));
#4703=DIRECTION('center_axis',(0.,-1.,0.));
#4704=DIRECTION('ref_axis',(1.,0.,0.));
#4705=DIRECTION('',(0.,-1.,0.));
#4706=DIRECTION('center_axis',(0.,-1.,0.));
#4707=DIRECTION('ref_axis',(1.,0.,0.));
#4708=DIRECTION('center_axis',(0.,1.,0.));
#4709=DIRECTION('ref_axis',(1.,0.,0.));
#4710=DIRECTION('center_axis',(0.,-1.,0.));
#4711=DIRECTION('ref_axis',(1.,0.,0.));
#4712=DIRECTION('center_axis',(0.,1.,0.));
#4713=DIRECTION('ref_axis',(1.,0.,0.));
#4714=DIRECTION('center_axis',(0.,-1.,0.));
#4715=DIRECTION('ref_axis',(1.,0.,0.));
#4716=DIRECTION('',(0.,-1.,0.));
#4717=DIRECTION('center_axis',(0.,1.,0.));
#4718=DIRECTION('ref_axis',(1.,0.,0.));
#4719=DIRECTION('center_axis',(0.,1.,0.));
#4720=DIRECTION('ref_axis',(1.,0.,0.));
#4721=DIRECTION('',(0.,-1.,0.));
#4722=DIRECTION('center_axis',(0.,1.,0.));
#4723=DIRECTION('ref_axis',(1.,0.,0.));
#4724=DIRECTION('center_axis',(0.,1.,0.));
#4725=DIRECTION('ref_axis',(1.,0.,0.));
#4726=DIRECTION('center_axis',(0.,1.,0.));
#4727=DIRECTION('ref_axis',(1.,0.,0.));
#5981=CARTESIAN_POINT('',(0.,0.,0.));
#5982=CARTESIAN_POINT('Origin',(-1.9,28.7,4.5));
#5983=CARTESIAN_POINT('',(-2.065,28.8,4.5));
#5984=CARTESIAN_POINT('Origin',(-1.9,28.8,4.5));
#5985=CARTESIAN_POINT('',(-2.065,30.,4.5));
#5986=CARTESIAN_POINT('',(-2.065,28.7,4.5));
#5987=CARTESIAN_POINT('Origin',(-1.9,30.,4.5));
#5988=CARTESIAN_POINT('Origin',(1.16341445918999E-16,28.7,6.4));
#5989=CARTESIAN_POINT('',(-0.165,28.8,6.4));
#5990=CARTESIAN_POINT('Origin',(1.16341445918999E-16,28.8,6.4));
#5991=CARTESIAN_POINT('',(-0.165,30.,6.4));
#5992=CARTESIAN_POINT('',(-0.165,28.7,6.4));
#5993=CARTESIAN_POINT('Origin',(1.16341445918999E-16,30.,6.4));
#5994=CARTESIAN_POINT('Origin',(1.9,28.7,4.5));
#5995=CARTESIAN_POINT('',(1.735,28.8,4.5));
#5996=CARTESIAN_POINT('Origin',(1.9,28.8,4.5));
#5997=CARTESIAN_POINT('',(1.735,30.,4.5));
#5998=CARTESIAN_POINT('',(1.735,28.7,4.5));
#5999=CARTESIAN_POINT('Origin',(1.9,30.,4.5));
#6000=CARTESIAN_POINT('Origin',(-3.49024337756996E-16,28.7,2.6));
#6001=CARTESIAN_POINT('',(-0.165,28.8,2.6));
#6002=CARTESIAN_POINT('Origin',(-3.49024337756996E-16,28.8,2.6));
#6003=CARTESIAN_POINT('',(-0.165,30.,2.6));
#6004=CARTESIAN_POINT('',(-0.165,28.7,2.6));
#6005=CARTESIAN_POINT('Origin',(-3.49024337756996E-16,30.,2.6));
#6006=CARTESIAN_POINT('Origin',(0.,28.8,4.5));
#6007=CARTESIAN_POINT('',(-1.2,29.1,4.5));
#6008=CARTESIAN_POINT('Origin',(0.,29.1,4.5));
#6009=CARTESIAN_POINT('',(-1.2,28.8,4.5));
#6010=CARTESIAN_POINT('',(-1.2,28.8,4.5));
#6011=CARTESIAN_POINT('Origin',(0.,28.8,4.5));
#6012=CARTESIAN_POINT('Origin',(0.,29.1,4.5));
#6013=CARTESIAN_POINT('',(-1.5,29.1,4.5));
#6014=CARTESIAN_POINT('Origin',(0.,29.1,4.5));
#6015=CARTESIAN_POINT('Origin',(0.,28.8,4.5));
#6016=CARTESIAN_POINT('',(-1.5,30.,4.5));
#6017=CARTESIAN_POINT('Origin',(0.,30.,4.5));
#6018=CARTESIAN_POINT('',(-1.5,28.8,4.5));
#6019=CARTESIAN_POINT('Origin',(0.,28.8,4.5));
#6020=CARTESIAN_POINT('',(-2.2,30.,4.5));
#6021=CARTESIAN_POINT('Origin',(0.,30.,4.5));
#6022=CARTESIAN_POINT('',(-2.2,28.8,4.5));
#6023=CARTESIAN_POINT('',(-2.2,28.8,4.5));
#6024=CARTESIAN_POINT('Origin',(0.,28.8,4.5));
#6025=CARTESIAN_POINT('Origin',(0.,30.,4.5));
#6026=CARTESIAN_POINT('Origin',(0.,28.8,4.5));
#6211=UNCERTAINTY_MEASURE_WITH_UNIT(LENGTH_MEASURE(0.001),#6242,
'DISTANCE_ACCURACY_VALUE',
'Maximum model space distance between geometric entities at asserted c
onnectivities');
#6215=UNCERTAINTY_MEASURE_WITH_UNIT(LENGTH_MEASURE(0.001),#6242,
'DISTANCE_ACCURACY_VALUE',
'Maximum model space distance between geometric entities at asserted c
onnectivities');
#6237=(
GEOMETRIC_REPRESENTATION_CONTEXT(3)
GLOBAL_UNCERTAINTY_ASSIGNED_CONTEXT((#6211))
GLOBAL_UNIT_ASSIGNED_CONTEXT((#6242,#6244,#6245))
REPRESENTATION_CONTEXT('','3D')
);
#6241=(
GEOMETRIC_REPRESENTATION_CONTEXT(3)
GLOBAL_UNCERTAINTY_ASSIGNED_CONTEXT((#6215))
GLOBAL_UNIT_ASSIGNED_CONTEXT((#6242,#6244,#6245))
REPRESENTATION_CONTEXT('','3D')
);
#6242=(
LENGTH_UNIT()
NAMED_UNIT(*)
SI_UNIT(.CENTI.,.METRE.)
);
#6244=(
NAMED_UNIT(*)
PLANE_ANGLE_UNIT()
SI_UNIT($,.RADIAN.)
);
#6245=(
NAMED_UNIT(*)
SI_UNIT($,.STERADIAN.)
SOLID_ANGLE_UNIT()
);
#6267=SHAPE_DEFINITION_REPRESENTATION(#6297,#6361);
#6297=PRODUCT_DEFINITION_SHAPE('',$,#6387);
#6361=SHAPE_REPRESENTATION('',(#3766),#6237);
#6365=PRODUCT_DEFINITION_CONTEXT('part definition',#6442,'design');
#6387=PRODUCT_DEFINITION('Bearing insert (1)','Bearing insert (1)',#6412,
#6365);
#6412=PRODUCT_DEFINITION_FORMATION('',$,#6465);
#6442=APPLICATION_CONTEXT(
'Core Data for Automotive Mechanical Design Process');
#6443=PRODUCT_CONTEXT('part definition',#6442,'mechanical');
#6465=PRODUCT('Bearing insert (1)','Bearing insert (1)','Bearing insert (1)',
(#6443));
#6532=COLOUR_RGB('Grey',0.48,0.52,0.57);
#6533=FILL_AREA_STYLE_COLOUR('',#6532);
#6534=FILL_AREA_STYLE('',(#6533));
#6535=SURFACE_STYLE_FILL_AREA(#6534);
#6536=SURFACE_SIDE_STYLE('',(#6535));
#6537=SURFACE_STYLE_USAGE(.BOTH.,#6536);
#6538=PRESENTATION_STYLE_ASSIGNMENT((#6537));
ENDSEC;
END-ISO-10303-21;
